ISO-10303-21;
HEADER;
/* Generated by software containing ST-Developer
 * from STEP Tools, Inc. (www.steptools.com) 
 */

FILE_DESCRIPTION(
/* description */ (''),
/* implementation_level */ '2;1');

FILE_NAME(
/* name */ 'Support_Block.step',
/* time_stamp */ '2026-10-19T02:00:06+06:00',
/* author */ (''),
/* organization */ (''),
/* preprocessor_version */ 'ST-DEVELOPER v20.2',
/* originating_system */ 'Autodesk Translation Framework v15.15.0.0',
/* authorisation */ '');

FILE_SCHEMA (('AUTOMOTIVE_DESIGN { 1 0 10303 214 3 1 1 }'));
ENDSEC;

DATA;
#10=MECHANICAL_DESIGN_GEOMETRIC_PRESENTATION_REPRESENTATION('',(#109),#4833);
#75=ELLIPSE('',#2918,1.08239220029239,1.);
#76=ELLIPSE('',#2919,1.0823922002924,1.);
#77=ELLIPSE('',#2921,1.08239220029239,1.);
#78=ELLIPSE('',#2923,1.08239220029239,1.);
#79=ELLIPSE('',#2924,1.0823922002924,1.);
#80=ELLIPSE('',#2927,1.0823922002924,1.);
#81=ELLIPSE('',#2929,1.08239220029239,1.);
#82=ELLIPSE('',#2931,1.08239220029239,1.);
#87=SHAPE_REPRESENTATION_RELATIONSHIP('SRR','None',#4878,#98);
#98=ADVANCED_BREP_SHAPE_REPRESENTATION('',(#120),#4826);
#109=STYLED_ITEM('',(#4971),#120);
#120=MANIFOLD_SOLID_BREP('Support_Block',#2691);
#200=PLANE('',#2933);
#201=PLANE('',#2934);
#202=PLANE('',#2935);
#203=PLANE('',#2936);
#204=PLANE('',#2937);
#205=PLANE('',#2938);
#206=PLANE('',#2939);
#207=PLANE('',#2940);
#208=PLANE('',#2941);
#209=PLANE('',#2942);
#210=PLANE('',#2943);
#211=PLANE('',#2944);
#325=FACE_OUTER_BOUND('',#498,.T.);
#326=FACE_OUTER_BOUND('',#499,.T.);
#327=FACE_OUTER_BOUND('',#500,.T.);
#328=FACE_OUTER_BOUND('',#501,.T.);
#329=FACE_OUTER_BOUND('',#502,.T.);
#330=FACE_OUTER_BOUND('',#503,.T.);
#331=FACE_OUTER_BOUND('',#504,.T.);
#332=FACE_OUTER_BOUND('',#505,.T.);
#333=FACE_OUTER_BOUND('',#506,.T.);
#334=FACE_OUTER_BOUND('',#507,.T.);
#335=FACE_OUTER_BOUND('',#508,.T.);
#336=FACE_OUTER_BOUND('',#509,.T.);
#337=FACE_OUTER_BOUND('',#510,.T.);
#338=FACE_OUTER_BOUND('',#511,.T.);
#339=FACE_OUTER_BOUND('',#512,.T.);
#340=FACE_OUTER_BOUND('',#513,.T.);
#341=FACE_OUTER_BOUND('',#514,.T.);
#342=FACE_OUTER_BOUND('',#515,.T.);
#343=FACE_OUTER_BOUND('',#516,.T.);
#344=FACE_OUTER_BOUND('',#517,.T.);
#498=EDGE_LOOP('',(#1983,#1984,#1985,#1986));
#499=EDGE_LOOP('',(#1987,#1988,#1989,#1990));
#500=EDGE_LOOP('',(#1991,#1992,#1993,#1994));
#501=EDGE_LOOP('',(#1995,#1996,#1997,#1998));
#502=EDGE_LOOP('',(#1999,#2000,#2001,#2002));
#503=EDGE_LOOP('',(#2003,#2004,#2005,#2006));
#504=EDGE_LOOP('',(#2007,#2008,#2009,#2010));
#505=EDGE_LOOP('',(#2011,#2012,#2013,#2014));
#506=EDGE_LOOP('',(#2015,#2016,#2017,#2018));
#507=EDGE_LOOP('',(#2019,#2020,#2021,#2022,#2023,#2024));
#508=EDGE_LOOP('',(#2025,#2026,#2027,#2028));
#509=EDGE_LOOP('',(#2029,#2030,#2031,#2032));
#510=EDGE_LOOP('',(#2033,#2034,#2035,#2036,#2037,#2038,#2039,#2040));
#511=EDGE_LOOP('',(#2041,#2042,#2043,#2044));
#512=EDGE_LOOP('',(#2045,#2046,#2047,#2048,#2049,#2050));
#513=EDGE_LOOP('',(#2051,#2052,#2053,#2054));
#514=EDGE_LOOP('',(#2055,#2056,#2057,#2058));
#515=EDGE_LOOP('',(#2059,#2060,#2061,#2062));
#516=EDGE_LOOP('',(#2063,#2064,#2065,#2066,#2067,#2068));
#517=EDGE_LOOP('',(#2069,#2070,#2071,#2072,#2073,#2074));
#696=LINE('',#4119,#950);
#697=LINE('',#4123,#951);
#698=LINE('',#4127,#952);
#699=LINE('',#4130,#953);
#700=LINE('',#4134,#954);
#701=LINE('',#4138,#955);
#702=LINE('',#4141,#956);
#703=LINE('',#4142,#957);
#704=LINE('',#4145,#958);
#705=LINE('',#4147,#959);
#706=LINE('',#4151,#960);
#707=LINE('',#4153,#961);
#708=LINE('',#4157,#962);
#709=LINE('',#4159,#963);
#710=LINE('',#4162,#964);
#711=LINE('',#4163,#965);
#712=LINE('',#4166,#966);
#713=LINE('',#4168,#967);
#714=LINE('',#4169,#968);
#715=LINE('',#4172,#969);
#716=LINE('',#4174,#970);
#717=LINE('',#4176,#971);
#718=LINE('',#4177,#972);
#719=LINE('',#4180,#973);
#720=LINE('',#4181,#974);
#721=LINE('',#4184,#975);
#722=LINE('',#4185,#976);
#723=LINE('',#4189,#977);
#724=LINE('',#4191,#978);
#725=LINE('',#4192,#979);
#726=LINE('',#4195,#980);
#727=LINE('',#4196,#981);
#728=LINE('',#4198,#982);
#729=LINE('',#4201,#983);
#730=LINE('',#4202,#984);
#731=LINE('',#4205,#985);
#732=LINE('',#4206,#986);
#733=LINE('',#4208,#987);
#950=VECTOR('',#3355,10.);
#951=VECTOR('',#3358,10.);
#952=VECTOR('',#3363,10.);
#953=VECTOR('',#3366,10.);
#954=VECTOR('',#3369,10.);
#955=VECTOR('',#3372,10.);
#956=VECTOR('',#3377,10.);
#957=VECTOR('',#3378,10.);
#958=VECTOR('',#3381,10.);
#959=VECTOR('',#3382,10.);
#960=VECTOR('',#3387,10.);
#961=VECTOR('',#3388,10.);
#962=VECTOR('',#3393,10.);
#963=VECTOR('',#3394,10.);
#964=VECTOR('',#3399,10.);
#965=VECTOR('',#3400,10.);
#966=VECTOR('',#3403,10.);
#967=VECTOR('',#3404,10.);
#968=VECTOR('',#3405,10.);
#969=VECTOR('',#3408,10.);
#970=VECTOR('',#3409,10.);
#971=VECTOR('',#3410,10.);
#972=VECTOR('',#3411,10.);
#973=VECTOR('',#3414,10.);
#974=VECTOR('',#3415,10.);
#975=VECTOR('',#3418,10.);
#976=VECTOR('',#3419,10.);
#977=VECTOR('',#3424,10.);
#978=VECTOR('',#3425,10.);
#979=VECTOR('',#3426,10.);
#980=VECTOR('',#3429,10.);
#981=VECTOR('',#3430,10.);
#982=VECTOR('',#3433,10.);
#983=VECTOR('',#3436,10.);
#984=VECTOR('',#3437,10.);
#985=VECTOR('',#3440,10.);
#986=VECTOR('',#3441,10.);
#987=VECTOR('',#3444,10.);
#1271=VERTEX_POINT('',#4117);
#1272=VERTEX_POINT('',#4118);
#1273=VERTEX_POINT('',#4120);
#1274=VERTEX_POINT('',#4122);
#1275=VERTEX_POINT('',#4126);
#1276=VERTEX_POINT('',#4128);
#1277=VERTEX_POINT('',#4132);
#1278=VERTEX_POINT('',#4133);
#1279=VERTEX_POINT('',#4135);
#1280=VERTEX_POINT('',#4137);
#1281=VERTEX_POINT('',#4144);
#1282=VERTEX_POINT('',#4146);
#1283=VERTEX_POINT('',#4150);
#1284=VERTEX_POINT('',#4152);
#1285=VERTEX_POINT('',#4156);
#1286=VERTEX_POINT('',#4158);
#1287=VERTEX_POINT('',#4165);
#1288=VERTEX_POINT('',#4167);
#1289=VERTEX_POINT('',#4171);
#1290=VERTEX_POINT('',#4173);
#1291=VERTEX_POINT('',#4175);
#1292=VERTEX_POINT('',#4179);
#1293=VERTEX_POINT('',#4183);
#1294=VERTEX_POINT('',#4188);
#1295=VERTEX_POINT('',#4190);
#1296=VERTEX_POINT('',#4194);
#1297=VERTEX_POINT('',#4200);
#1298=VERTEX_POINT('',#4204);
#1532=EDGE_CURVE('',#1271,#1272,#696,.T.);
#1533=EDGE_CURVE('',#1272,#1273,#75,.T.);
#1534=EDGE_CURVE('',#1273,#1274,#697,.T.);
#1535=EDGE_CURVE('',#1271,#1274,#76,.T.);
#1536=EDGE_CURVE('',#1272,#1275,#698,.T.);
#1537=EDGE_CURVE('',#1275,#1276,#77,.T.);
#1538=EDGE_CURVE('',#1276,#1273,#699,.T.);
#1539=EDGE_CURVE('',#1277,#1278,#700,.T.);
#1540=EDGE_CURVE('',#1278,#1279,#78,.T.);
#1541=EDGE_CURVE('',#1279,#1280,#701,.T.);
#1542=EDGE_CURVE('',#1280,#1277,#79,.T.);
#1543=EDGE_CURVE('',#1275,#1279,#702,.T.);
#1544=EDGE_CURVE('',#1278,#1276,#703,.T.);
#1545=EDGE_CURVE('',#1281,#1277,#704,.T.);
#1546=EDGE_CURVE('',#1280,#1282,#705,.T.);
#1547=EDGE_CURVE('',#1282,#1281,#80,.T.);
#1548=EDGE_CURVE('',#1283,#1281,#706,.T.);
#1549=EDGE_CURVE('',#1282,#1284,#707,.T.);
#1550=EDGE_CURVE('',#1284,#1283,#81,.T.);
#1551=EDGE_CURVE('',#1285,#1283,#708,.T.);
#1552=EDGE_CURVE('',#1284,#1286,#709,.T.);
#1553=EDGE_CURVE('',#1286,#1285,#82,.T.);
#1554=EDGE_CURVE('',#1274,#1285,#710,.T.);
#1555=EDGE_CURVE('',#1286,#1271,#711,.T.);
#1556=EDGE_CURVE('',#1273,#1287,#712,.T.);
#1557=EDGE_CURVE('',#1288,#1287,#713,.T.);
#1558=EDGE_CURVE('',#1274,#1288,#714,.T.);
#1559=EDGE_CURVE('',#1276,#1289,#715,.T.);
#1560=EDGE_CURVE('',#1289,#1290,#716,.T.);
#1561=EDGE_CURVE('',#1290,#1291,#717,.T.);
#1562=EDGE_CURVE('',#1287,#1291,#718,.T.);
#1563=EDGE_CURVE('',#1278,#1292,#719,.T.);
#1564=EDGE_CURVE('',#1292,#1289,#720,.T.);
#1565=EDGE_CURVE('',#1277,#1293,#721,.T.);
#1566=EDGE_CURVE('',#1293,#1292,#722,.T.);
#1567=EDGE_CURVE('',#1291,#1294,#723,.T.);
#1568=EDGE_CURVE('',#1290,#1295,#724,.T.);
#1569=EDGE_CURVE('',#1294,#1295,#725,.T.);
#1570=EDGE_CURVE('',#1296,#1293,#726,.T.);
#1571=EDGE_CURVE('',#1295,#1296,#727,.T.);
#1572=EDGE_CURVE('',#1281,#1296,#728,.T.);
#1573=EDGE_CURVE('',#1297,#1288,#729,.T.);
#1574=EDGE_CURVE('',#1285,#1297,#730,.T.);
#1575=EDGE_CURVE('',#1298,#1297,#731,.T.);
#1576=EDGE_CURVE('',#1283,#1298,#732,.T.);
#1577=EDGE_CURVE('',#1294,#1298,#733,.T.);
#1983=ORIENTED_EDGE('',*,*,#1532,.T.);
#1984=ORIENTED_EDGE('',*,*,#1533,.T.);
#1985=ORIENTED_EDGE('',*,*,#1534,.T.);
#1986=ORIENTED_EDGE('',*,*,#1535,.F.);
#1987=ORIENTED_EDGE('',*,*,#1536,.T.);
#1988=ORIENTED_EDGE('',*,*,#1537,.T.);
#1989=ORIENTED_EDGE('',*,*,#1538,.T.);
#1990=ORIENTED_EDGE('',*,*,#1533,.F.);
#1991=ORIENTED_EDGE('',*,*,#1539,.T.);
#1992=ORIENTED_EDGE('',*,*,#1540,.T.);
#1993=ORIENTED_EDGE('',*,*,#1541,.T.);
#1994=ORIENTED_EDGE('',*,*,#1542,.T.);
#1995=ORIENTED_EDGE('',*,*,#1543,.T.);
#1996=ORIENTED_EDGE('',*,*,#1540,.F.);
#1997=ORIENTED_EDGE('',*,*,#1544,.T.);
#1998=ORIENTED_EDGE('',*,*,#1537,.F.);
#1999=ORIENTED_EDGE('',*,*,#1545,.T.);
#2000=ORIENTED_EDGE('',*,*,#1542,.F.);
#2001=ORIENTED_EDGE('',*,*,#1546,.T.);
#2002=ORIENTED_EDGE('',*,*,#1547,.T.);
#2003=ORIENTED_EDGE('',*,*,#1548,.T.);
#2004=ORIENTED_EDGE('',*,*,#1547,.F.);
#2005=ORIENTED_EDGE('',*,*,#1549,.T.);
#2006=ORIENTED_EDGE('',*,*,#1550,.T.);
#2007=ORIENTED_EDGE('',*,*,#1551,.T.);
#2008=ORIENTED_EDGE('',*,*,#1550,.F.);
#2009=ORIENTED_EDGE('',*,*,#1552,.T.);
#2010=ORIENTED_EDGE('',*,*,#1553,.T.);
#2011=ORIENTED_EDGE('',*,*,#1554,.T.);
#2012=ORIENTED_EDGE('',*,*,#1553,.F.);
#2013=ORIENTED_EDGE('',*,*,#1555,.T.);
#2014=ORIENTED_EDGE('',*,*,#1535,.T.);
#2015=ORIENTED_EDGE('',*,*,#1534,.F.);
#2016=ORIENTED_EDGE('',*,*,#1556,.T.);
#2017=ORIENTED_EDGE('',*,*,#1557,.F.);
#2018=ORIENTED_EDGE('',*,*,#1558,.F.);
#2019=ORIENTED_EDGE('',*,*,#1538,.F.);
#2020=ORIENTED_EDGE('',*,*,#1559,.T.);
#2021=ORIENTED_EDGE('',*,*,#1560,.T.);
#2022=ORIENTED_EDGE('',*,*,#1561,.T.);
#2023=ORIENTED_EDGE('',*,*,#1562,.F.);
#2024=ORIENTED_EDGE('',*,*,#1556,.F.);
#2025=ORIENTED_EDGE('',*,*,#1544,.F.);
#2026=ORIENTED_EDGE('',*,*,#1563,.T.);
#2027=ORIENTED_EDGE('',*,*,#1564,.T.);
#2028=ORIENTED_EDGE('',*,*,#1559,.F.);
#2029=ORIENTED_EDGE('',*,*,#1539,.F.);
#2030=ORIENTED_EDGE('',*,*,#1565,.T.);
#2031=ORIENTED_EDGE('',*,*,#1566,.T.);
#2032=ORIENTED_EDGE('',*,*,#1563,.F.);
#2033=ORIENTED_EDGE('',*,*,#1541,.F.);
#2034=ORIENTED_EDGE('',*,*,#1543,.F.);
#2035=ORIENTED_EDGE('',*,*,#1536,.F.);
#2036=ORIENTED_EDGE('',*,*,#1532,.F.);
#2037=ORIENTED_EDGE('',*,*,#1555,.F.);
#2038=ORIENTED_EDGE('',*,*,#1552,.F.);
#2039=ORIENTED_EDGE('',*,*,#1549,.F.);
#2040=ORIENTED_EDGE('',*,*,#1546,.F.);
#2041=ORIENTED_EDGE('',*,*,#1567,.F.);
#2042=ORIENTED_EDGE('',*,*,#1561,.F.);
#2043=ORIENTED_EDGE('',*,*,#1568,.T.);
#2044=ORIENTED_EDGE('',*,*,#1569,.F.);
#2045=ORIENTED_EDGE('',*,*,#1564,.F.);
#2046=ORIENTED_EDGE('',*,*,#1566,.F.);
#2047=ORIENTED_EDGE('',*,*,#1570,.F.);
#2048=ORIENTED_EDGE('',*,*,#1571,.F.);
#2049=ORIENTED_EDGE('',*,*,#1568,.F.);
#2050=ORIENTED_EDGE('',*,*,#1560,.F.);
#2051=ORIENTED_EDGE('',*,*,#1545,.F.);
#2052=ORIENTED_EDGE('',*,*,#1572,.T.);
#2053=ORIENTED_EDGE('',*,*,#1570,.T.);
#2054=ORIENTED_EDGE('',*,*,#1565,.F.);
#2055=ORIENTED_EDGE('',*,*,#1554,.F.);
#2056=ORIENTED_EDGE('',*,*,#1558,.T.);
#2057=ORIENTED_EDGE('',*,*,#1573,.F.);
#2058=ORIENTED_EDGE('',*,*,#1574,.F.);
#2059=ORIENTED_EDGE('',*,*,#1551,.F.);
#2060=ORIENTED_EDGE('',*,*,#1574,.T.);
#2061=ORIENTED_EDGE('',*,*,#1575,.F.);
#2062=ORIENTED_EDGE('',*,*,#1576,.F.);
#2063=ORIENTED_EDGE('',*,*,#1548,.F.);
#2064=ORIENTED_EDGE('',*,*,#1576,.T.);
#2065=ORIENTED_EDGE('',*,*,#1577,.F.);
#2066=ORIENTED_EDGE('',*,*,#1569,.T.);
#2067=ORIENTED_EDGE('',*,*,#1571,.T.);
#2068=ORIENTED_EDGE('',*,*,#1572,.F.);
#2069=ORIENTED_EDGE('',*,*,#1567,.T.);
#2070=ORIENTED_EDGE('',*,*,#1577,.T.);
#2071=ORIENTED_EDGE('',*,*,#1575,.T.);
#2072=ORIENTED_EDGE('',*,*,#1573,.T.);
#2073=ORIENTED_EDGE('',*,*,#1557,.T.);
#2074=ORIENTED_EDGE('',*,*,#1562,.T.);
#2494=CYLINDRICAL_SURFACE('',#2917,1.);
#2495=CYLINDRICAL_SURFACE('',#2920,1.);
#2496=CYLINDRICAL_SURFACE('',#2922,1.);
#2497=CYLINDRICAL_SURFACE('',#2925,1.);
#2498=CYLINDRICAL_SURFACE('',#2926,1.);
#2499=CYLINDRICAL_SURFACE('',#2928,1.);
#2500=CYLINDRICAL_SURFACE('',#2930,1.);
#2501=CYLINDRICAL_SURFACE('',#2932,1.);
#2583=ADVANCED_FACE('',(#325),#2494,.T.);
#2584=ADVANCED_FACE('',(#326),#2495,.T.);
#2585=ADVANCED_FACE('',(#327),#2496,.T.);
#2586=ADVANCED_FACE('',(#328),#2497,.T.);
#2587=ADVANCED_FACE('',(#329),#2498,.T.);
#2588=ADVANCED_FACE('',(#330),#2499,.T.);
#2589=ADVANCED_FACE('',(#331),#2500,.T.);
#2590=ADVANCED_FACE('',(#332),#2501,.T.);
#2591=ADVANCED_FACE('',(#333),#200,.T.);
#2592=ADVANCED_FACE('',(#334),#201,.T.);
#2593=ADVANCED_FACE('',(#335),#202,.T.);
#2594=ADVANCED_FACE('',(#336),#203,.T.);
#2595=ADVANCED_FACE('',(#337),#204,.F.);
#2596=ADVANCED_FACE('',(#338),#205,.F.);
#2597=ADVANCED_FACE('',(#339),#206,.F.);
#2598=ADVANCED_FACE('',(#340),#207,.T.);
#2599=ADVANCED_FACE('',(#341),#208,.T.);
#2600=ADVANCED_FACE('',(#342),#209,.T.);
#2601=ADVANCED_FACE('',(#343),#210,.T.);
#2602=ADVANCED_FACE('',(#344),#211,.T.);
#2691=CLOSED_SHELL('',(#2583,#2584,#2585,#2586,#2587,#2588,#2589,#2590,
#2591,#2592,#2593,#2594,#2595,#2596,#2597,#2598,#2599,#2600,#2601,#2602));
#2916=AXIS2_PLACEMENT_3D('',#4115,#3351,#3352);
#2917=AXIS2_PLACEMENT_3D('',#4116,#3353,#3354);
#2918=AXIS2_PLACEMENT_3D('',#4121,#3356,#3357);
#2919=AXIS2_PLACEMENT_3D('',#4124,#3359,#3360);
#2920=AXIS2_PLACEMENT_3D('',#4125,#3361,#3362);
#2921=AXIS2_PLACEMENT_3D('',#4129,#3364,#3365);
#2922=AXIS2_PLACEMENT_3D('',#4131,#3367,#3368);
#2923=AXIS2_PLACEMENT_3D('',#4136,#3370,#3371);
#2924=AXIS2_PLACEMENT_3D('',#4139,#3373,#3374);
#2925=AXIS2_PLACEMENT_3D('',#4140,#3375,#3376);
#2926=AXIS2_PLACEMENT_3D('',#4143,#3379,#3380);
#2927=AXIS2_PLACEMENT_3D('',#4148,#3383,#3384);
#2928=AXIS2_PLACEMENT_3D('',#4149,#3385,#3386);
#2929=AXIS2_PLACEMENT_3D('',#4154,#3389,#3390);
#2930=AXIS2_PLACEMENT_3D('',#4155,#3391,#3392);
#2931=AXIS2_PLACEMENT_3D('',#4160,#3395,#3396);
#2932=AXIS2_PLACEMENT_3D('',#4161,#3397,#3398);
#2933=AXIS2_PLACEMENT_3D('',#4164,#3401,#3402);
#2934=AXIS2_PLACEMENT_3D('',#4170,#3406,#3407);
#2935=AXIS2_PLACEMENT_3D('',#4178,#3412,#3413);
#2936=AXIS2_PLACEMENT_3D('',#4182,#3416,#3417);
#2937=AXIS2_PLACEMENT_3D('',#4186,#3420,#3421);
#2938=AXIS2_PLACEMENT_3D('',#4187,#3422,#3423);
#2939=AXIS2_PLACEMENT_3D('',#4193,#3427,#3428);
#2940=AXIS2_PLACEMENT_3D('',#4197,#3431,#3432);
#2941=AXIS2_PLACEMENT_3D('',#4199,#3434,#3435);
#2942=AXIS2_PLACEMENT_3D('',#4203,#3438,#3439);
#2943=AXIS2_PLACEMENT_3D('',#4207,#3442,#3443);
#2944=AXIS2_PLACEMENT_3D('',#4209,#3445,#3446);
#3351=DIRECTION('axis',(0.,0.,1.));
#3352=DIRECTION('refdir',(1.,0.,0.));
#3353=DIRECTION('center_axis',(0.,0.707106781186548,0.707106781186548));
#3354=DIRECTION('ref_axis',(0.707106781186541,-0.500000000000005,0.500000000000005));
#3355=DIRECTION('',(0.,0.707106781186548,0.707106781186548));
#3356=DIRECTION('center_axis',(0.,-0.923879532511287,-0.38268343236509));
#3357=DIRECTION('ref_axis',(0.,0.38268343236509,-0.923879532511287));
#3358=DIRECTION('',(0.,-0.707106781186548,-0.707106781186548));
#3359=DIRECTION('center_axis',(-2.05142465794792E-15,-0.382683432365092,
-0.923879532511286));
#3360=DIRECTION('ref_axis',(4.95257723140443E-15,0.923879532511286,-0.382683432365092));
#3361=DIRECTION('center_axis',(0.,1.,0.));
#3362=DIRECTION('ref_axis',(0.70710678118654,0.,0.707106781186555));
#3363=DIRECTION('',(0.,1.,0.));
#3364=DIRECTION('center_axis',(4.24863957754293E-15,-0.923879532511293,
0.382683432365076));
#3365=DIRECTION('ref_axis',(-1.02571232897397E-14,-0.382683432365076,-0.923879532511292));
#3366=DIRECTION('',(0.,-1.,0.));
#3367=DIRECTION('center_axis',(0.,0.,-1.));
#3368=DIRECTION('ref_axis',(0.707106781186548,0.707106781186548,0.));
#3369=DIRECTION('',(0.,0.,1.));
#3370=DIRECTION('center_axis',(0.,0.382683432365083,-0.92387953251129));
#3371=DIRECTION('ref_axis',(0.,0.92387953251129,0.382683432365083));
#3372=DIRECTION('',(0.,0.,-1.));
#3373=DIRECTION('center_axis',(0.,0.382683432365092,0.923879532511286));
#3374=DIRECTION('ref_axis',(0.,-0.923879532511286,0.382683432365092));
#3375=DIRECTION('center_axis',(0.,0.707106781186547,-0.707106781186548));
#3376=DIRECTION('ref_axis',(0.707106781186543,0.500000000000006,0.5));
#3377=DIRECTION('',(0.,0.707106781186547,-0.707106781186548));
#3378=DIRECTION('',(0.,-0.707106781186547,0.707106781186548));
#3379=DIRECTION('center_axis',(0.,-0.707106781186548,-0.707106781186548));
#3380=DIRECTION('ref_axis',(0.707106781186541,0.500000000000005,-0.500000000000005));
#3381=DIRECTION('',(0.,0.707106781186548,0.707106781186548));
#3382=DIRECTION('',(0.,-0.707106781186548,-0.707106781186548));
#3383=DIRECTION('center_axis',(0.,0.923879532511293,0.382683432365075));
#3384=DIRECTION('ref_axis',(0.,-0.382683432365075,0.923879532511293));
#3385=DIRECTION('center_axis',(0.,-1.,2.61228946970625E-17));
#3386=DIRECTION('ref_axis',(0.70710678118654,0.,-0.707106781186555));
#3387=DIRECTION('',(0.,1.,-2.61228946970625E-17));
#3388=DIRECTION('',(0.,-1.,2.61228946970625E-17));
#3389=DIRECTION('center_axis',(-1.7261125179092E-14,0.923879532511293,-0.382683432365076));
#3390=DIRECTION('ref_axis',(4.16720425091855E-14,0.382683432365076,0.923879532511292));
#3391=DIRECTION('center_axis',(0.,-0.707106781186548,0.707106781186547));
#3392=DIRECTION('ref_axis',(0.707106781186541,-0.500000000000005,-0.500000000000005));
#3393=DIRECTION('',(0.,0.707106781186548,-0.707106781186547));
#3394=DIRECTION('',(0.,-0.707106781186548,0.707106781186547));
#3395=DIRECTION('center_axis',(0.,0.382683432365092,-0.923879532511286));
#3396=DIRECTION('ref_axis',(0.,0.923879532511286,0.382683432365092));
#3397=DIRECTION('center_axis',(0.,0.,1.));
#3398=DIRECTION('ref_axis',(0.707106781186548,-0.707106781186548,0.));
#3399=DIRECTION('',(0.,0.,-1.));
#3400=DIRECTION('',(0.,0.,1.));
#3401=DIRECTION('center_axis',(0.,-0.707106781186548,0.707106781186548));
#3402=DIRECTION('ref_axis',(0.,0.707106781186548,0.707106781186548));
#3403=DIRECTION('',(-1.,0.,0.));
#3404=DIRECTION('',(0.,0.707106781186547,0.707106781186547));
#3405=DIRECTION('',(-1.,0.,0.));
#3406=DIRECTION('center_axis',(0.,0.,1.));
#3407=DIRECTION('ref_axis',(0.,1.,0.));
#3408=DIRECTION('',(-1.,0.,0.));
#3409=DIRECTION('',(0.,-1.,0.));
#3410=DIRECTION('',(-1.,0.,0.));
#3411=DIRECTION('',(0.,1.,0.));
#3412=DIRECTION('center_axis',(0.,0.707106781186548,0.707106781186547));
#3413=DIRECTION('ref_axis',(0.,0.707106781186547,-0.707106781186548));
#3414=DIRECTION('',(-1.,0.,0.));
#3415=DIRECTION('',(0.,-0.707106781186547,0.707106781186548));
#3416=DIRECTION('center_axis',(0.,1.,0.));
#3417=DIRECTION('ref_axis',(0.,0.,-1.));
#3418=DIRECTION('',(-1.,0.,0.));
#3419=DIRECTION('',(0.,0.,1.));
#3420=DIRECTION('center_axis',(-1.,0.,0.));
#3421=DIRECTION('ref_axis',(0.,-1.,0.));
#3422=DIRECTION('center_axis',(0.,-1.,0.));
#3423=DIRECTION('ref_axis',(0.,0.,-1.));
#3424=DIRECTION('',(0.,0.,-1.));
#3425=DIRECTION('',(0.,0.,-1.));
#3426=DIRECTION('',(1.,0.,0.));
#3427=DIRECTION('center_axis',(1.,0.,0.));
#3428=DIRECTION('ref_axis',(0.,0.,-1.));
#3429=DIRECTION('',(0.,0.707106781186548,0.707106781186548));
#3430=DIRECTION('',(0.,1.,-2.61228946970625E-17));
#3431=DIRECTION('center_axis',(0.,0.707106781186548,-0.707106781186548));
#3432=DIRECTION('ref_axis',(0.,-0.707106781186548,-0.707106781186548));
#3433=DIRECTION('',(-1.,0.,0.));
#3434=DIRECTION('center_axis',(0.,-1.,0.));
#3435=DIRECTION('ref_axis',(0.,0.,1.));
#3436=DIRECTION('',(0.,0.,1.));
#3437=DIRECTION('',(-1.,0.,0.));
#3438=DIRECTION('center_axis',(0.,-0.707106781186547,-0.707106781186548));
#3439=DIRECTION('ref_axis',(0.,-0.707106781186548,0.707106781186547));
#3440=DIRECTION('',(0.,-0.707106781186548,0.707106781186547));
#3441=DIRECTION('',(-1.,0.,0.));
#3442=DIRECTION('center_axis',(0.,-2.61228946970625E-17,-1.));
#3443=DIRECTION('ref_axis',(0.,-1.,2.61228946970625E-17));
#3444=DIRECTION('',(0.,-1.,2.61228946970625E-17));
#3445=DIRECTION('center_axis',(-1.,0.,0.));
#3446=DIRECTION('ref_axis',(0.,0.,1.));
#4115=CARTESIAN_POINT('',(0.,0.,0.));
#4116=CARTESIAN_POINT('Origin',(89.,-70.542893218824,33.0428932188156));
#4117=CARTESIAN_POINT('',(90.,-89.0000000000105,14.585786437629));
#4118=CARTESIAN_POINT('',(90.,-84.5857864376374,19.0000000000021));
#4119=CARTESIAN_POINT('',(90.,-70.542893218824,33.0428932188156));
#4120=CARTESIAN_POINT('',(89.,-85.0000000000105,20.0000000000021));
#4121=CARTESIAN_POINT('Origin',(89.,-84.5857864376374,19.0000000000021));
#4122=CARTESIAN_POINT('',(89.,-90.0000000000105,15.0000000000021));
#4123=CARTESIAN_POINT('',(89.,-71.2500000000105,33.7500000000021));
#4124=CARTESIAN_POINT('Origin',(89.,-89.0000000000105,14.585786437629));
#4125=CARTESIAN_POINT('Origin',(89.,-42.5000000000105,19.0000000000021));
#4126=CARTESIAN_POINT('',(90.,84.5857864376164,19.0000000000021));
#4127=CARTESIAN_POINT('',(90.,-42.5000000000105,19.0000000000021));
#4128=CARTESIAN_POINT('',(89.,84.9999999999895,20.0000000000021));
#4129=CARTESIAN_POINT('Origin',(89.,84.5857864376164,19.0000000000021));
#4130=CARTESIAN_POINT('',(89.,-42.5000000000105,20.0000000000021));
#4131=CARTESIAN_POINT('Origin',(89.,88.9999999999895,7.50000000000211));
#4132=CARTESIAN_POINT('',(89.,89.9999999999895,-14.9999999999979));
#4133=CARTESIAN_POINT('',(89.,89.9999999999895,15.0000000000021));
#4134=CARTESIAN_POINT('',(89.,89.9999999999895,7.50000000000211));
#4135=CARTESIAN_POINT('',(90.,88.9999999999895,14.585786437629));
#4136=CARTESIAN_POINT('Origin',(89.,88.9999999999895,14.585786437629));
#4137=CARTESIAN_POINT('',(90.,88.9999999999895,-14.5857864376248));
#4138=CARTESIAN_POINT('',(90.,88.9999999999895,7.50000000000211));
#4139=CARTESIAN_POINT('Origin',(89.,88.9999999999895,-14.5857864376248));
#4140=CARTESIAN_POINT('Origin',(89.,68.042893218803,35.5428932188156));
#4141=CARTESIAN_POINT('',(90.,68.042893218803,35.5428932188156));
#4142=CARTESIAN_POINT('',(89.,68.7499999999895,36.2500000000021));
#4143=CARTESIAN_POINT('Origin',(89.,70.5428932188029,-33.0428932188113));
#4144=CARTESIAN_POINT('',(89.,84.9999999999895,-19.9999999999979));
#4145=CARTESIAN_POINT('',(89.,71.2499999999895,-33.7499999999979));
#4146=CARTESIAN_POINT('',(90.,84.5857864376164,-18.9999999999979));
#4147=CARTESIAN_POINT('',(90.,70.5428932188029,-33.0428932188113));
#4148=CARTESIAN_POINT('Origin',(89.,84.5857864376164,-18.9999999999979));
#4149=CARTESIAN_POINT('Origin',(89.,42.4999999999895,-18.9999999999979));
#4150=CARTESIAN_POINT('',(89.,-85.0000000000105,-19.9999999999979));
#4151=CARTESIAN_POINT('',(89.,42.4999999999895,-19.9999999999979));
#4152=CARTESIAN_POINT('',(90.,-84.5857864376374,-18.9999999999979));
#4153=CARTESIAN_POINT('',(90.,42.4999999999895,-18.9999999999979));
#4154=CARTESIAN_POINT('Origin',(89.,-84.5857864376374,-18.9999999999979));
#4155=CARTESIAN_POINT('Origin',(89.,-68.042893218824,-35.5428932188113));
#4156=CARTESIAN_POINT('',(89.,-90.0000000000105,-14.9999999999979));
#4157=CARTESIAN_POINT('',(89.,-68.7500000000105,-36.2499999999979));
#4158=CARTESIAN_POINT('',(90.,-89.0000000000105,-14.5857864376248));
#4159=CARTESIAN_POINT('',(90.,-68.042893218824,-35.5428932188113));
#4160=CARTESIAN_POINT('Origin',(89.,-89.0000000000105,-14.5857864376248));
#4161=CARTESIAN_POINT('Origin',(89.,-89.0000000000105,-7.49999999999789));
#4162=CARTESIAN_POINT('',(89.,-90.0000000000105,-7.49999999999789));
#4163=CARTESIAN_POINT('',(90.,-89.0000000000105,-7.49999999999789));
#4164=CARTESIAN_POINT('Origin',(90.,-90.0000000000105,15.0000000000021));
#4165=CARTESIAN_POINT('',(70.,-85.0000000000105,20.0000000000021));
#4166=CARTESIAN_POINT('',(90.,-85.0000000000105,20.0000000000021));
#4167=CARTESIAN_POINT('',(70.,-90.0000000000105,15.0000000000021));
#4168=CARTESIAN_POINT('',(70.,-90.0000000000105,15.0000000000021));
#4169=CARTESIAN_POINT('',(90.,-90.0000000000105,15.0000000000021));
#4170=CARTESIAN_POINT('Origin',(90.,-85.0000000000105,20.0000000000021));
#4171=CARTESIAN_POINT('',(85.,84.9999999999895,20.0000000000021));
#4172=CARTESIAN_POINT('',(90.,84.9999999999895,20.0000000000021));
#4173=CARTESIAN_POINT('',(85.,29.9999999999895,20.0000000000021));
#4174=CARTESIAN_POINT('',(85.,-12.5000000000105,20.0000000000021));
#4175=CARTESIAN_POINT('',(70.,29.9999999999895,20.0000000000021));
#4176=CARTESIAN_POINT('',(80.,29.9999999999895,20.0000000000021));
#4177=CARTESIAN_POINT('',(70.,-85.0000000000105,20.0000000000021));
#4178=CARTESIAN_POINT('Origin',(90.,84.9999999999895,20.0000000000021));
#4179=CARTESIAN_POINT('',(85.,89.9999999999895,15.0000000000021));
#4180=CARTESIAN_POINT('',(90.,89.9999999999895,15.0000000000021));
#4181=CARTESIAN_POINT('',(85.,83.7499999999895,21.2500000000021));
#4182=CARTESIAN_POINT('Origin',(90.,89.9999999999895,15.0000000000021));
#4183=CARTESIAN_POINT('',(85.,89.9999999999895,-14.9999999999979));
#4184=CARTESIAN_POINT('',(90.,89.9999999999895,-14.9999999999979));
#4185=CARTESIAN_POINT('',(85.,89.9999999999895,7.50000000000211));
#4186=CARTESIAN_POINT('Origin',(90.,-1.05160324892495E-11,2.11275441586167E-12));
#4187=CARTESIAN_POINT('Origin',(70.,29.9999999999895,20.0000000000021));
#4188=CARTESIAN_POINT('',(70.,29.9999999999895,-19.9999999999979));
#4189=CARTESIAN_POINT('',(70.,29.9999999999895,10.0000000000021));
#4190=CARTESIAN_POINT('',(85.,29.9999999999895,-19.9999999999979));
#4191=CARTESIAN_POINT('',(85.,29.9999999999895,20.0000000000021));
#4192=CARTESIAN_POINT('',(80.,29.9999999999895,-19.9999999999979));
#4193=CARTESIAN_POINT('Origin',(85.,59.9999999999895,2.1138646388863E-12));
#4194=CARTESIAN_POINT('',(85.,84.9999999999895,-19.9999999999979));
#4195=CARTESIAN_POINT('',(85.,86.2499999999895,-18.7499999999979));
#4196=CARTESIAN_POINT('',(85.,72.4999999999895,-19.9999999999979));
#4197=CARTESIAN_POINT('Origin',(90.,89.9999999999895,-14.9999999999979));
#4198=CARTESIAN_POINT('',(90.,84.9999999999895,-19.9999999999979));
#4199=CARTESIAN_POINT('Origin',(90.,-90.0000000000105,-14.9999999999979));
#4200=CARTESIAN_POINT('',(70.,-90.0000000000105,-14.9999999999979));
#4201=CARTESIAN_POINT('',(70.,-90.0000000000105,-14.9999999999979));
#4202=CARTESIAN_POINT('',(90.,-90.0000000000105,-14.9999999999979));
#4203=CARTESIAN_POINT('Origin',(90.,-85.0000000000105,-19.9999999999979));
#4204=CARTESIAN_POINT('',(70.,-85.0000000000105,-19.9999999999979));
#4205=CARTESIAN_POINT('',(70.,-85.0000000000105,-19.9999999999979));
#4206=CARTESIAN_POINT('',(90.,-85.0000000000105,-19.9999999999979));
#4207=CARTESIAN_POINT('Origin',(90.,84.9999999999895,-19.9999999999979));
#4208=CARTESIAN_POINT('',(70.,84.9999999999895,-19.9999999999979));
#4209=CARTESIAN_POINT('Origin',(70.,-1.05160324892495E-11,2.11164419283705E-12));
#4813=UNCERTAINTY_MEASURE_WITH_UNIT(LENGTH_MEASURE(0.01),#4834,
'DISTANCE_ACCURACY_VALUE',
'Maximum model space distance between geometric entities at asserted c
onnectivities');
#4820=UNCERTAINTY_MEASURE_WITH_UNIT(LENGTH_MEASURE(0.01),#4834,
'DISTANCE_ACCURACY_VALUE',
'Maximum model space distance between geometric entities at asserted c
onnectivities');
#4826=(
GEOMETRIC_REPRESENTATION_CONTEXT(3)
GLOBAL_UNCERTAINTY_ASSIGNED_CONTEXT((#4813))
GLOBAL_UNIT_ASSIGNED_CONTEXT((#4834,#4836,#4837))
REPRESENTATION_CONTEXT('','3D')
);
#4833=(
GEOMETRIC_REPRESENTATION_CONTEXT(3)
GLOBAL_UNCERTAINTY_ASSIGNED_CONTEXT((#4820))
GLOBAL_UNIT_ASSIGNED_CONTEXT((#4834,#4836,#4837))
REPRESENTATION_CONTEXT('','3D')
);
#4834=(
LENGTH_UNIT()
NAMED_UNIT(*)
SI_UNIT(.MILLI.,.METRE.)
);
#4836=(
NAMED_UNIT(*)
PLANE_ANGLE_UNIT()
SI_UNIT($,.RADIAN.)
);
#4837=(
NAMED_UNIT(*)
SI_UNIT($,.STERADIAN.)
SOLID_ANGLE_UNIT()
);
#4843=SHAPE_DEFINITION_REPRESENTATION(#4855,#4878);
#4855=PRODUCT_DEFINITION_SHAPE('',$,#4891);
#4878=SHAPE_REPRESENTATION('',(#2916),#4826);
#4885=PRODUCT_DEFINITION_CONTEXT('part definition',#4923,'design');
#4891=PRODUCT_DEFINITION('Support_Block','Support_Block',#4903,#4885);
#4903=PRODUCT_DEFINITION_FORMATION('',$,#4930);
#4923=APPLICATION_CONTEXT(
'Core Data for Automotive Mechanical Design Process');
#4924=PRODUCT_CONTEXT('part definition',#4923,'mechanical');
#4930=PRODUCT('Support_Block','Support_Block',$,(#4924));
#4965=COLOUR_RGB('Dark Blue',0.08,0.2,0.34);
#4966=FILL_AREA_STYLE_COLOUR('',#4965);
#4967=FILL_AREA_STYLE('',(#4966));
#4968=SURFACE_STYLE_FILL_AREA(#4967);
#4969=SURFACE_SIDE_STYLE('',(#4968));
#4970=SURFACE_STYLE_USAGE(.BOTH.,#4969);
#4971=PRESENTATION_STYLE_ASSIGNMENT((#4970));
ENDSEC;
END-ISO-10303-21;
